ISO-10303-21;
HEADER;
FILE_DESCRIPTION((''),'2;1');
FILE_NAME('Washer_2.step','2026-10-09T11:34:15-07:00',(''),(''),'','','');
FILE_SCHEMA (('AUTOMOTIVE_DESIGN { 1 0 10303 214 3 1 1 }'));
ENDSEC;
DATA;
#10=MECHANICAL_DESIGN_GEOMETRIC_PRESENTATION_REPRESENTATION('',(#638),#117170);
#315=ELLIPSE('',#52193,0.14142135623731,0.1) ;
#316=ELLIPSE('',#52209,0.141421356237297,0.1) ;
#596=SHAPE_REPRESENTATION_RELATIONSHIP('SRR','None',#117251,#617) ;
#617=ADVANCED_BREP_SHAPE_REPRESENTATION('',(#659),#117159) ;
#638=STYLED_ITEM('',(#117355),#659) ;
#659=MANIFOLD_SOLID_BREP('Body1',#49067) ;
#2199=SPHERICAL_SURFACE('',#52180,0.0999999999999979) ;
#2200=SPHERICAL_SURFACE('',#52184,0.100000000000016) ;
#2201=SPHERICAL_SURFACE('',#52188,0.100000000000016) ;
#2202=SPHERICAL_SURFACE('',#52195,0.0999999999999979) ;
#2203=SPHERICAL_SURFACE('',#52199,0.0999999999999979) ;
#2501=PLANE('',#52213) ;
#2502=PLANE('',#52214) ;
#2503=PLANE('',#52215) ;
#2504=PLANE('',#52216) ;
#2505=PLANE('',#52217) ;
#2506=PLANE('',#52218) ;
#4344=LINE('',#88143,#7558) ;
#4345=LINE('',#88145,#7559) ;
#4346=LINE('',#88148,#7560) ;
#4347=LINE('',#88149,#7561) ;
#4348=LINE('',#88165,#7562) ;
#4349=LINE('',#88166,#7563) ;
#4350=LINE('',#88168,#7564) ;
#4351=LINE('',#88169,#7565) ;
#4352=LINE('',#88174,#7566) ;
#4353=LINE('',#88175,#7567) ;
#4354=LINE('',#88177,#7568) ;
#4355=LINE('',#88178,#7569) ;
#4356=LINE('',#88181,#7570) ;
#4357=LINE('',#88183,#7571) ;
#4358=LINE('',#88186,#7572) ;
#4359=LINE('',#88187,#7573) ;
#4360=LINE('',#88189,#7574) ;
#4361=LINE('',#88190,#7575) ;
#4362=LINE('',#88192,#7576) ;
#4363=LINE('',#88193,#7577) ;
#4364=LINE('',#88195,#7578) ;
#4365=LINE('',#88197,#7579) ;
#7558=VECTOR('',#62175,10.) ;
#7559=VECTOR('',#62176,10.) ;
#7560=VECTOR('',#62181,10.) ;
#7561=VECTOR('',#62182,10.) ;
#7562=VECTOR('',#62201,10.) ;
#7563=VECTOR('',#62202,10.) ;
#7564=VECTOR('',#62205,10.) ;
#7565=VECTOR('',#62206,10.) ;
#7566=VECTOR('',#62211,10.) ;
#7567=VECTOR('',#62212,10.) ;
#7568=VECTOR('',#62215,10.) ;
#7569=VECTOR('',#62216,10.) ;
#7570=VECTOR('',#62219,10.) ;
#7571=VECTOR('',#62220,10.) ;
#7572=VECTOR('',#62225,10.) ;
#7573=VECTOR('',#62226,10.) ;
#7574=VECTOR('',#62229,10.) ;
#7575=VECTOR('',#62230,10.) ;
#7576=VECTOR('',#62233,10.) ;
#7577=VECTOR('',#62234,10.) ;
#7578=VECTOR('',#62237,10.) ;
#7579=VECTOR('',#62240,10.) ;
#10030=CYLINDRICAL_SURFACE('',#52192,0.1) ;
#10031=CYLINDRICAL_SURFACE('',#52194,0.1) ;
#10032=CYLINDRICAL_SURFACE('',#52203,0.1) ;
#10033=CYLINDRICAL_SURFACE('',#52204,0.1) ;
#10034=CYLINDRICAL_SURFACE('',#52205,0.1) ;
#10035=CYLINDRICAL_SURFACE('',#52207,0.1) ;
#10036=CYLINDRICAL_SURFACE('',#52208,0.1) ;
#10037=CYLINDRICAL_SURFACE('',#52210,0.1) ;
#10038=CYLINDRICAL_SURFACE('',#52211,0.1) ;
#10039=CYLINDRICAL_SURFACE('',#52212,0.1) ;
#12194=FACE_OUTER_BOUND('',#15350,.T.) ;
#12195=FACE_OUTER_BOUND('',#15351,.T.) ;
#12196=FACE_OUTER_BOUND('',#15352,.T.) ;
#12197=FACE_OUTER_BOUND('',#15353,.T.) ;
#12198=FACE_OUTER_BOUND('',#15354,.T.) ;
#12199=FACE_OUTER_BOUND('',#15355,.T.) ;
#12200=FACE_OUTER_BOUND('',#15356,.T.) ;
#12201=FACE_OUTER_BOUND('',#15357,.T.) ;
#12202=FACE_OUTER_BOUND('',#15358,.T.) ;
#12203=FACE_OUTER_BOUND('',#15359,.T.) ;
#12204=FACE_OUTER_BOUND('',#15360,.T.) ;
#12205=FACE_OUTER_BOUND('',#15361,.T.) ;
#12206=FACE_OUTER_BOUND('',#15362,.T.) ;
#12207=FACE_OUTER_BOUND('',#15363,.T.) ;
#12208=FACE_OUTER_BOUND('',#15364,.T.) ;
#12209=FACE_OUTER_BOUND('',#15365,.T.) ;
#12210=FACE_OUTER_BOUND('',#15366,.T.) ;
#12211=FACE_OUTER_BOUND('',#15367,.T.) ;
#12212=FACE_OUTER_BOUND('',#15368,.T.) ;
#12213=FACE_OUTER_BOUND('',#15369,.T.) ;
#12214=FACE_OUTER_BOUND('',#15370,.T.) ;
#15350=EDGE_LOOP('',(#37662,#37663,#37664)) ;
#15351=EDGE_LOOP('',(#37665,#37666,#37667)) ;
#15352=EDGE_LOOP('',(#37668,#37669,#37670)) ;
#15353=EDGE_LOOP('',(#37671,#37672,#37673,#37674)) ;
#15354=EDGE_LOOP('',(#37675,#37676,#37677,#37678)) ;
#15355=EDGE_LOOP('',(#37679,#37680,#37681)) ;
#15356=EDGE_LOOP('',(#37682,#37683,#37684)) ;
#15357=EDGE_LOOP('',(#37685,#37686,#37687,#37688)) ;
#15358=EDGE_LOOP('',(#37689,#37690,#37691,#37692)) ;
#15359=EDGE_LOOP('',(#37693,#37694,#37695,#37696)) ;
#15360=EDGE_LOOP('',(#37697,#37698,#37699,#37700)) ;
#15361=EDGE_LOOP('',(#37701,#37702,#37703,#37704)) ;
#15362=EDGE_LOOP('',(#37705,#37706,#37707,#37708)) ;
#15363=EDGE_LOOP('',(#37709,#37710,#37711,#37712)) ;
#15364=EDGE_LOOP('',(#37713,#37714,#37715,#37716)) ;
#15365=EDGE_LOOP('',(#37717,#37718,#37719,#37720)) ;
#15366=EDGE_LOOP('',(#37721,#37722,#37723,#37724)) ;
#15367=EDGE_LOOP('',(#37725,#37726,#37727,#37728)) ;
#15368=EDGE_LOOP('',(#37729,#37730,#37731,#37732)) ;
#15369=EDGE_LOOP('',(#37733,#37734,#37735,#37736)) ;
#15370=EDGE_LOOP('',(#37737,#37738,#37739,#37740,#37741)) ;
#18469=CIRCLE('',#52181,0.100000000000016) ;
#18470=CIRCLE('',#52182,0.0999999999999979) ;
#18471=CIRCLE('',#52183,0.0999999999999979) ;
#18472=CIRCLE('',#52185,0.0999999999999979) ;
#18473=CIRCLE('',#52186,0.100000000000016) ;
#18474=CIRCLE('',#52187,0.0999999999999979) ;
#18475=CIRCLE('',#52189,0.0999999999999979) ;
#18476=CIRCLE('',#52190,0.100000000000016) ;
#18477=CIRCLE('',#52191,0.0999999999999979) ;
#18478=CIRCLE('',#52196,0.100000000000016) ;
#18479=CIRCLE('',#52197,0.0999999999999979) ;
#18480=CIRCLE('',#52198,0.0999999999999979) ;
#18481=CIRCLE('',#52200,0.0999999999999979) ;
#18482=CIRCLE('',#52201,0.0999999999999979) ;
#18483=CIRCLE('',#52202,0.100000000000051) ;
#18484=CIRCLE('',#52206,0.1) ;
#21486=VERTEX_POINT('',#88121) ;
#21487=VERTEX_POINT('',#88122) ;
#21488=VERTEX_POINT('',#88124) ;
#21489=VERTEX_POINT('',#88128) ;
#21490=VERTEX_POINT('',#88129) ;
#21491=VERTEX_POINT('',#88131) ;
#21492=VERTEX_POINT('',#88135) ;
#21493=VERTEX_POINT('',#88136) ;
#21494=VERTEX_POINT('',#88138) ;
#21495=VERTEX_POINT('',#88142) ;
#21496=VERTEX_POINT('',#88144) ;
#21497=VERTEX_POINT('',#88151) ;
#21498=VERTEX_POINT('',#88152) ;
#21499=VERTEX_POINT('',#88154) ;
#21500=VERTEX_POINT('',#88158) ;
#21501=VERTEX_POINT('',#88159) ;
#21502=VERTEX_POINT('',#88161) ;
#21503=VERTEX_POINT('',#88171) ;
#21504=VERTEX_POINT('',#88172) ;
#21505=VERTEX_POINT('',#88180) ;
#21506=VERTEX_POINT('',#88182) ;
#27109=EDGE_CURVE('',#21486,#21487,#18469,.F.) ;
#27110=EDGE_CURVE('',#21488,#21486,#18470,.F.) ;
#27111=EDGE_CURVE('',#21487,#21488,#18471,.F.) ;
#27112=EDGE_CURVE('',#21489,#21490,#18472,.F.) ;
#27113=EDGE_CURVE('',#21491,#21489,#18473,.F.) ;
#27114=EDGE_CURVE('',#21490,#21491,#18474,.F.) ;
#27115=EDGE_CURVE('',#21492,#21493,#18475,.F.) ;
#27116=EDGE_CURVE('',#21494,#21492,#18476,.F.) ;
#27117=EDGE_CURVE('',#21493,#21494,#18477,.F.) ;
#27118=EDGE_CURVE('',#21495,#21494,#4344,.T.) ;
#27119=EDGE_CURVE('',#21492,#21496,#4345,.T.) ;
#27120=EDGE_CURVE('',#21496,#21495,#315,.T.) ;
#27121=EDGE_CURVE('',#21489,#21493,#4346,.T.) ;
#27122=EDGE_CURVE('',#21494,#21491,#4347,.T.) ;
#27123=EDGE_CURVE('',#21497,#21498,#18478,.F.) ;
#27124=EDGE_CURVE('',#21499,#21497,#18479,.F.) ;
#27125=EDGE_CURVE('',#21498,#21499,#18480,.F.) ;
#27126=EDGE_CURVE('',#21500,#21501,#18481,.F.) ;
#27127=EDGE_CURVE('',#21502,#21500,#18482,.F.) ;
#27128=EDGE_CURVE('',#21501,#21502,#18483,.F.) ;
#27129=EDGE_CURVE('',#21500,#21492,#4348,.T.) ;
#27130=EDGE_CURVE('',#21493,#21502,#4349,.T.) ;
#27131=EDGE_CURVE('',#21497,#21501,#4350,.T.) ;
#27132=EDGE_CURVE('',#21502,#21499,#4351,.T.) ;
#27133=EDGE_CURVE('',#21503,#21504,#18484,.T.) ;
#27134=EDGE_CURVE('',#21504,#21500,#4352,.T.) ;
#27135=EDGE_CURVE('',#21501,#21503,#4353,.T.) ;
#27136=EDGE_CURVE('',#21490,#21498,#4354,.T.) ;
#27137=EDGE_CURVE('',#21499,#21489,#4355,.T.) ;
#27138=EDGE_CURVE('',#21505,#21497,#4356,.T.) ;
#27139=EDGE_CURVE('',#21498,#21506,#4357,.T.) ;
#27140=EDGE_CURVE('',#21506,#21505,#316,.T.) ;
#27141=EDGE_CURVE('',#21487,#21490,#4358,.T.) ;
#27142=EDGE_CURVE('',#21491,#21486,#4359,.T.) ;
#27143=EDGE_CURVE('',#21506,#21487,#4360,.T.) ;
#27144=EDGE_CURVE('',#21488,#21505,#4361,.T.) ;
#27145=EDGE_CURVE('',#21496,#21488,#4362,.T.) ;
#27146=EDGE_CURVE('',#21486,#21495,#4363,.T.) ;
#27147=EDGE_CURVE('',#21496,#21504,#4364,.T.) ;
#27148=EDGE_CURVE('',#21503,#21505,#4365,.T.) ;
#37662=ORIENTED_EDGE('',*,*,#27109,.F.) ;
#37663=ORIENTED_EDGE('',*,*,#27110,.F.) ;
#37664=ORIENTED_EDGE('',*,*,#27111,.F.) ;
#37665=ORIENTED_EDGE('',*,*,#27112,.F.) ;
#37666=ORIENTED_EDGE('',*,*,#27113,.F.) ;
#37667=ORIENTED_EDGE('',*,*,#27114,.F.) ;
#37668=ORIENTED_EDGE('',*,*,#27115,.F.) ;
#37669=ORIENTED_EDGE('',*,*,#27116,.F.) ;
#37670=ORIENTED_EDGE('',*,*,#27117,.F.) ;
#37671=ORIENTED_EDGE('',*,*,#27118,.T.) ;
#37672=ORIENTED_EDGE('',*,*,#27116,.T.) ;
#37673=ORIENTED_EDGE('',*,*,#27119,.T.) ;
#37674=ORIENTED_EDGE('',*,*,#27120,.T.) ;
#37675=ORIENTED_EDGE('',*,*,#27113,.T.) ;
#37676=ORIENTED_EDGE('',*,*,#27121,.T.) ;
#37677=ORIENTED_EDGE('',*,*,#27117,.T.) ;
#37678=ORIENTED_EDGE('',*,*,#27122,.T.) ;
#37679=ORIENTED_EDGE('',*,*,#27123,.F.) ;
#37680=ORIENTED_EDGE('',*,*,#27124,.F.) ;
#37681=ORIENTED_EDGE('',*,*,#27125,.F.) ;
#37682=ORIENTED_EDGE('',*,*,#27126,.F.) ;
#37683=ORIENTED_EDGE('',*,*,#27127,.F.) ;
#37684=ORIENTED_EDGE('',*,*,#27128,.F.) ;
#37685=ORIENTED_EDGE('',*,*,#27127,.T.) ;
#37686=ORIENTED_EDGE('',*,*,#27129,.T.) ;
#37687=ORIENTED_EDGE('',*,*,#27115,.T.) ;
#37688=ORIENTED_EDGE('',*,*,#27130,.T.) ;
#37689=ORIENTED_EDGE('',*,*,#27124,.T.) ;
#37690=ORIENTED_EDGE('',*,*,#27131,.T.) ;
#37691=ORIENTED_EDGE('',*,*,#27128,.T.) ;
#37692=ORIENTED_EDGE('',*,*,#27132,.T.) ;
#37693=ORIENTED_EDGE('',*,*,#27133,.T.) ;
#37694=ORIENTED_EDGE('',*,*,#27134,.T.) ;
#37695=ORIENTED_EDGE('',*,*,#27126,.T.) ;
#37696=ORIENTED_EDGE('',*,*,#27135,.T.) ;
#37697=ORIENTED_EDGE('',*,*,#27112,.T.) ;
#37698=ORIENTED_EDGE('',*,*,#27136,.T.) ;
#37699=ORIENTED_EDGE('',*,*,#27125,.T.) ;
#37700=ORIENTED_EDGE('',*,*,#27137,.T.) ;
#37701=ORIENTED_EDGE('',*,*,#27138,.T.) ;
#37702=ORIENTED_EDGE('',*,*,#27123,.T.) ;
#37703=ORIENTED_EDGE('',*,*,#27139,.T.) ;
#37704=ORIENTED_EDGE('',*,*,#27140,.T.) ;
#37705=ORIENTED_EDGE('',*,*,#27109,.T.) ;
#37706=ORIENTED_EDGE('',*,*,#27141,.T.) ;
#37707=ORIENTED_EDGE('',*,*,#27114,.T.) ;
#37708=ORIENTED_EDGE('',*,*,#27142,.T.) ;
#37709=ORIENTED_EDGE('',*,*,#27143,.T.) ;
#37710=ORIENTED_EDGE('',*,*,#27111,.T.) ;
#37711=ORIENTED_EDGE('',*,*,#27144,.T.) ;
#37712=ORIENTED_EDGE('',*,*,#27140,.F.) ;
#37713=ORIENTED_EDGE('',*,*,#27145,.T.) ;
#37714=ORIENTED_EDGE('',*,*,#27110,.T.) ;
#37715=ORIENTED_EDGE('',*,*,#27146,.T.) ;
#37716=ORIENTED_EDGE('',*,*,#27120,.F.) ;
#37717=ORIENTED_EDGE('',*,*,#27119,.F.) ;
#37718=ORIENTED_EDGE('',*,*,#27129,.F.) ;
#37719=ORIENTED_EDGE('',*,*,#27134,.F.) ;
#37720=ORIENTED_EDGE('',*,*,#27147,.F.) ;
#37721=ORIENTED_EDGE('',*,*,#27135,.F.) ;
#37722=ORIENTED_EDGE('',*,*,#27131,.F.) ;
#37723=ORIENTED_EDGE('',*,*,#27138,.F.) ;
#37724=ORIENTED_EDGE('',*,*,#27148,.F.) ;
#37725=ORIENTED_EDGE('',*,*,#27118,.F.) ;
#37726=ORIENTED_EDGE('',*,*,#27146,.F.) ;
#37727=ORIENTED_EDGE('',*,*,#27142,.F.) ;
#37728=ORIENTED_EDGE('',*,*,#27122,.F.) ;
#37729=ORIENTED_EDGE('',*,*,#27121,.F.) ;
#37730=ORIENTED_EDGE('',*,*,#27137,.F.) ;
#37731=ORIENTED_EDGE('',*,*,#27132,.F.) ;
#37732=ORIENTED_EDGE('',*,*,#27130,.F.) ;
#37733=ORIENTED_EDGE('',*,*,#27136,.F.) ;
#37734=ORIENTED_EDGE('',*,*,#27141,.F.) ;
#37735=ORIENTED_EDGE('',*,*,#27143,.F.) ;
#37736=ORIENTED_EDGE('',*,*,#27139,.F.) ;
#37737=ORIENTED_EDGE('',*,*,#27145,.F.) ;
#37738=ORIENTED_EDGE('',*,*,#27147,.T.) ;
#37739=ORIENTED_EDGE('',*,*,#27133,.F.) ;
#37740=ORIENTED_EDGE('',*,*,#27148,.T.) ;
#37741=ORIENTED_EDGE('',*,*,#27144,.F.) ;
#47412=ADVANCED_FACE('',(#12194),#2199,.T.) ;
#47413=ADVANCED_FACE('',(#12195),#2200,.T.) ;
#47414=ADVANCED_FACE('',(#12196),#2201,.T.) ;
#47415=ADVANCED_FACE('',(#12197),#10030,.T.) ;
#47416=ADVANCED_FACE('',(#12198),#10031,.T.) ;
#47417=ADVANCED_FACE('',(#12199),#2202,.T.) ;
#47418=ADVANCED_FACE('',(#12200),#2203,.T.) ;
#47419=ADVANCED_FACE('',(#12201),#10032,.T.) ;
#47420=ADVANCED_FACE('',(#12202),#10033,.T.) ;
#47421=ADVANCED_FACE('',(#12203),#10034,.T.) ;
#47422=ADVANCED_FACE('',(#12204),#10035,.T.) ;
#47423=ADVANCED_FACE('',(#12205),#10036,.T.) ;
#47424=ADVANCED_FACE('',(#12206),#10037,.T.) ;
#47425=ADVANCED_FACE('',(#12207),#10038,.T.) ;
#47426=ADVANCED_FACE('',(#12208),#10039,.T.) ;
#47427=ADVANCED_FACE('',(#12209),#2501,.T.) ;
#47428=ADVANCED_FACE('',(#12210),#2502,.T.) ;
#47429=ADVANCED_FACE('',(#12211),#2503,.T.) ;
#47430=ADVANCED_FACE('',(#12212),#2504,.T.) ;
#47431=ADVANCED_FACE('',(#12213),#2505,.T.) ;
#47432=ADVANCED_FACE('',(#12214),#2506,.T.) ;
#49067=CLOSED_SHELL('',(#47412,#47413,#47414,#47415,#47416,#47417,#47418,
#47419,#47420,#47421,#47422,#47423,#47424,#47425,#47426,#47427,#47428,#47429,
#47430,#47431,#47432)) ;
#52179=AXIS2_PLACEMENT_3D('',#88119,#62147,#62148) ;
#52180=AXIS2_PLACEMENT_3D('',#88120,#62149,#62150) ;
#52181=AXIS2_PLACEMENT_3D('',#88123,#62151,#62152) ;
#52182=AXIS2_PLACEMENT_3D('',#88125,#62153,#62154) ;
#52183=AXIS2_PLACEMENT_3D('',#88126,#62155,#62156) ;
#52184=AXIS2_PLACEMENT_3D('',#88127,#62157,#62158) ;
#52185=AXIS2_PLACEMENT_3D('',#88130,#62159,#62160) ;
#52186=AXIS2_PLACEMENT_3D('',#88132,#62161,#62162) ;
#52187=AXIS2_PLACEMENT_3D('',#88133,#62163,#62164) ;
#52188=AXIS2_PLACEMENT_3D('',#88134,#62165,#62166) ;
#52189=AXIS2_PLACEMENT_3D('',#88137,#62167,#62168) ;
#52190=AXIS2_PLACEMENT_3D('',#88139,#62169,#62170) ;
#52191=AXIS2_PLACEMENT_3D('',#88140,#62171,#62172) ;
#52192=AXIS2_PLACEMENT_3D('',#88141,#62173,#62174) ;
#52193=AXIS2_PLACEMENT_3D('',#88146,#62177,#62178) ;
#52194=AXIS2_PLACEMENT_3D('',#88147,#62179,#62180) ;
#52195=AXIS2_PLACEMENT_3D('',#88150,#62183,#62184) ;
#52196=AXIS2_PLACEMENT_3D('',#88153,#62185,#62186) ;
#52197=AXIS2_PLACEMENT_3D('',#88155,#62187,#62188) ;
#52198=AXIS2_PLACEMENT_3D('',#88156,#62189,#62190) ;
#52199=AXIS2_PLACEMENT_3D('',#88157,#62191,#62192) ;
#52200=AXIS2_PLACEMENT_3D('',#88160,#62193,#62194) ;
#52201=AXIS2_PLACEMENT_3D('',#88162,#62195,#62196) ;
#52202=AXIS2_PLACEMENT_3D('',#88163,#62197,#62198) ;
#52203=AXIS2_PLACEMENT_3D('',#88164,#62199,#62200) ;
#52204=AXIS2_PLACEMENT_3D('',#88167,#62203,#62204) ;
#52205=AXIS2_PLACEMENT_3D('',#88170,#62207,#62208) ;
#52206=AXIS2_PLACEMENT_3D('',#88173,#62209,#62210) ;
#52207=AXIS2_PLACEMENT_3D('',#88176,#62213,#62214) ;
#52208=AXIS2_PLACEMENT_3D('',#88179,#62217,#62218) ;
#52209=AXIS2_PLACEMENT_3D('',#88184,#62221,#62222) ;
#52210=AXIS2_PLACEMENT_3D('',#88185,#62223,#62224) ;
#52211=AXIS2_PLACEMENT_3D('',#88188,#62227,#62228) ;
#52212=AXIS2_PLACEMENT_3D('',#88191,#62231,#62232) ;
#52213=AXIS2_PLACEMENT_3D('',#88194,#62235,#62236) ;
#52214=AXIS2_PLACEMENT_3D('',#88196,#62238,#62239) ;
#52215=AXIS2_PLACEMENT_3D('',#88198,#62241,#62242) ;
#52216=AXIS2_PLACEMENT_3D('',#88199,#62243,#62244) ;
#52217=AXIS2_PLACEMENT_3D('',#88200,#62245,#62246) ;
#52218=AXIS2_PLACEMENT_3D('',#88201,#62247,#62248) ;
#62147=DIRECTION('axis',(0.,0.,1.)) ;
#62148=DIRECTION('refdir',(1.,0.,0.)) ;
#62149=DIRECTION('center_axis',(-0.81649658092788,0.408248290463869,0.408248290463549)) ;
#62150=DIRECTION('ref_axis',(0.577350269189413,0.577350269190052,0.577350269189413)) ;
#62151=DIRECTION('center_axis',(0.,0.,1.)) ;
#62152=DIRECTION('ref_axis',(0.,1.,0.)) ;
#62153=DIRECTION('center_axis',(1.,0.,0.)) ;
#62154=DIRECTION('ref_axis',(0.,0.,1.)) ;
#62155=DIRECTION('center_axis',(0.,1.,3.55271367880058E-13)) ;
#62156=DIRECTION('ref_axis',(1.,0.,0.)) ;
#62157=DIRECTION('center_axis',(-0.816496580927773,0.408248290463798,-0.408248290463833)) ;
#62158=DIRECTION('ref_axis',(0.577350269189567,0.577350269189673,-0.577350269189638)) ;
#62159=DIRECTION('center_axis',(0.,1.,0.)) ;
#62160=DIRECTION('ref_axis',(0.,0.,-1.)) ;
#62161=DIRECTION('center_axis',(1.,0.,0.)) ;
#62162=DIRECTION('ref_axis',(0.,1.,0.)) ;
#62163=DIRECTION('center_axis',(0.,0.,-1.)) ;
#62164=DIRECTION('ref_axis',(1.,0.,0.)) ;
#62165=DIRECTION('center_axis',(-0.816496580927773,-0.408248290463798,0.408248290463833)) ;
#62166=DIRECTION('ref_axis',(-0.577350269189567,0.577350269189673,-0.577350269189638)) ;
#62167=DIRECTION('center_axis',(0.,1.,0.)) ;
#62168=DIRECTION('ref_axis',(-1.,0.,0.)) ;
#62169=DIRECTION('center_axis',(0.,0.,-1.)) ;
#62170=DIRECTION('ref_axis',(0.,1.,0.)) ;
#62171=DIRECTION('center_axis',(-1.,0.,0.)) ;
#62172=DIRECTION('ref_axis',(0.,0.,-1.)) ;
#62173=DIRECTION('center_axis',(0.,0.,-1.)) ;
#62174=DIRECTION('ref_axis',(-0.70710678118661,0.707106781186485,0.)) ;
#62175=DIRECTION('',(0.,0.,-1.)) ;
#62176=DIRECTION('',(0.,0.,1.)) ;
#62177=DIRECTION('center_axis',(-0.707106781186548,0.,-0.707106781186548)) ;
#62178=DIRECTION('ref_axis',(-0.707106781186547,0.,0.707106781186547)) ;
#62179=DIRECTION('center_axis',(1.,0.,0.)) ;
#62180=DIRECTION('ref_axis',(0.,0.707106781186485,-0.70710678118661)) ;
#62181=DIRECTION('',(-1.,0.,0.)) ;
#62182=DIRECTION('',(1.,0.,0.)) ;
#62183=DIRECTION('center_axis',(-0.81649658092788,-0.408248290463869,-0.408248290463549)) ;
#62184=DIRECTION('ref_axis',(0.577350269189413,-0.577350269190052,-0.577350269189413)) ;
#62185=DIRECTION('center_axis',(0.,0.,-1.)) ;
#62186=DIRECTION('ref_axis',(0.,-1.,0.)) ;
#62187=DIRECTION('center_axis',(1.,0.,0.)) ;
#62188=DIRECTION('ref_axis',(0.,0.,-1.)) ;
#62189=DIRECTION('center_axis',(0.,-1.,-3.55271367880058E-13)) ;
#62190=DIRECTION('ref_axis',(1.,0.,0.)) ;
#62191=DIRECTION('center_axis',(-0.81649658092788,0.408248290463869,0.408248290463549)) ;
#62192=DIRECTION('ref_axis',(-0.577350269189413,-0.577350269190052,-0.577350269189413)) ;
#62193=DIRECTION('center_axis',(0.,0.,-1.)) ;
#62194=DIRECTION('ref_axis',(-1.,0.,0.)) ;
#62195=DIRECTION('center_axis',(3.55271367880058E-13,-1.,0.)) ;
#62196=DIRECTION('ref_axis',(0.,0.,-1.)) ;
#62197=DIRECTION('center_axis',(-1.,0.,0.)) ;
#62198=DIRECTION('ref_axis',(0.,-1.,0.)) ;
#62199=DIRECTION('center_axis',(0.,-1.,0.)) ;
#62200=DIRECTION('ref_axis',(-0.707106781186548,0.,-0.707106781186548)) ;
#62201=DIRECTION('',(0.,1.,0.)) ;
#62202=DIRECTION('',(0.,-1.,0.)) ;
#62203=DIRECTION('center_axis',(1.,0.,0.)) ;
#62204=DIRECTION('ref_axis',(0.,-0.707106781186736,-0.707106781186359)) ;
#62205=DIRECTION('',(-1.,0.,0.)) ;
#62206=DIRECTION('',(1.,0.,0.)) ;
#62207=DIRECTION('center_axis',(0.,0.,1.)) ;
#62208=DIRECTION('ref_axis',(-0.70710678118661,-0.707106781186485,0.)) ;
#62209=DIRECTION('center_axis',(0.,0.,-1.)) ;
#62210=DIRECTION('ref_axis',(-0.70710678118661,-0.707106781186485,0.)) ;
#62211=DIRECTION('',(0.,0.,-1.)) ;
#62212=DIRECTION('',(0.,0.,1.)) ;
#62213=DIRECTION('center_axis',(0.,1.,0.)) ;
#62214=DIRECTION('ref_axis',(0.707106781186548,0.,-0.707106781186548)) ;
#62215=DIRECTION('',(0.,-1.,0.)) ;
#62216=DIRECTION('',(0.,1.,0.)) ;
#62217=DIRECTION('center_axis',(0.,0.,-1.)) ;
#62218=DIRECTION('ref_axis',(0.70710678118661,-0.707106781186485,0.)) ;
#62219=DIRECTION('',(0.,0.,-1.)) ;
#62220=DIRECTION('',(0.,0.,1.)) ;
#62221=DIRECTION('center_axis',(0.,-0.707106781186485,-0.70710678118661)) ;
#62222=DIRECTION('ref_axis',(0.,-0.70710678118661,0.707106781186485)) ;
#62223=DIRECTION('center_axis',(0.,0.,1.)) ;
#62224=DIRECTION('ref_axis',(0.70710678118661,0.707106781186485,0.)) ;
#62225=DIRECTION('',(0.,0.,-1.)) ;
#62226=DIRECTION('',(0.,0.,1.)) ;
#62227=DIRECTION('center_axis',(0.,-1.,0.)) ;
#62228=DIRECTION('ref_axis',(0.707106781186548,0.,0.707106781186548)) ;
#62229=DIRECTION('',(0.,1.,0.)) ;
#62230=DIRECTION('',(0.,-1.,0.)) ;
#62231=DIRECTION('center_axis',(1.,0.,0.)) ;
#62232=DIRECTION('ref_axis',(0.,0.707106781186736,0.707106781186359)) ;
#62233=DIRECTION('',(1.,0.,0.)) ;
#62234=DIRECTION('',(-1.,0.,0.)) ;
#62235=DIRECTION('center_axis',(-1.,0.,0.)) ;
#62236=DIRECTION('ref_axis',(0.,-1.,0.)) ;
#62237=DIRECTION('',(0.,-1.,0.)) ;
#62238=DIRECTION('center_axis',(0.,-1.,0.)) ;
#62239=DIRECTION('ref_axis',(0.,0.,-1.)) ;
#62240=DIRECTION('',(1.,0.,0.)) ;
#62241=DIRECTION('center_axis',(0.,1.,0.)) ;
#62242=DIRECTION('ref_axis',(0.,0.,1.)) ;
#62243=DIRECTION('center_axis',(0.,0.,-1.)) ;
#62244=DIRECTION('ref_axis',(0.,1.,0.)) ;
#62245=DIRECTION('center_axis',(1.,0.,0.)) ;
#62246=DIRECTION('ref_axis',(0.,0.,-1.)) ;
#62247=DIRECTION('center_axis',(0.,0.,1.)) ;
#62248=DIRECTION('ref_axis',(0.,-1.,0.)) ;
#88119=CARTESIAN_POINT('',(0.,0.,0.)) ;
#88120=CARTESIAN_POINT('Origin',(28.,248.1,26.6213203435596)) ;
#88121=CARTESIAN_POINT('',(28.,248.2,26.6213203435596)) ;
#88122=CARTESIAN_POINT('',(28.1,248.1,26.6213203435596)) ;
#88123=CARTESIAN_POINT('Origin',(28.,248.1,26.6213203435596)) ;
#88124=CARTESIAN_POINT('',(28.,248.1,26.7213203435596)) ;
#88125=CARTESIAN_POINT('Origin',(28.,248.1,26.6213203435596)) ;
#88126=CARTESIAN_POINT('Origin',(28.,248.1,26.6213203435596)) ;
#88127=CARTESIAN_POINT('Origin',(28.,248.1,26.1213203435596)) ;
#88128=CARTESIAN_POINT('',(28.,248.1,26.0213203435596)) ;
#88129=CARTESIAN_POINT('',(28.1,248.1,26.1213203435596)) ;
#88130=CARTESIAN_POINT('Origin',(28.,248.1,26.1213203435596)) ;
#88131=CARTESIAN_POINT('',(28.,248.2,26.1213203435596)) ;
#88132=CARTESIAN_POINT('Origin',(28.,248.1,26.1213203435596)) ;
#88133=CARTESIAN_POINT('Origin',(28.,248.1,26.1213203435596)) ;
#88134=CARTESIAN_POINT('Origin',(26.4,248.1,26.1213203435596)) ;
#88135=CARTESIAN_POINT('',(26.3,248.1,26.1213203435596)) ;
#88136=CARTESIAN_POINT('',(26.4,248.1,26.0213203435596)) ;
#88137=CARTESIAN_POINT('Origin',(26.4,248.1,26.1213203435596)) ;
#88138=CARTESIAN_POINT('',(26.4,248.2,26.1213203435596)) ;
#88139=CARTESIAN_POINT('Origin',(26.4,248.1,26.1213203435596)) ;
#88140=CARTESIAN_POINT('Origin',(26.4,248.1,26.1213203435596)) ;
#88141=CARTESIAN_POINT('Origin',(26.4,248.1,26.1963203435596)) ;
#88142=CARTESIAN_POINT('',(26.4,248.2,26.6213203435596)) ;
#88143=CARTESIAN_POINT('',(26.4,248.2,26.1963203435596)) ;
#88144=CARTESIAN_POINT('',(26.3,248.1,26.7213203435596)) ;
#88145=CARTESIAN_POINT('',(26.3,248.1,26.1963203435596)) ;
#88146=CARTESIAN_POINT('Origin',(26.4,248.1,26.6213203435596)) ;
#88147=CARTESIAN_POINT('Origin',(26.3,248.1,26.1213203435596)) ;
#88148=CARTESIAN_POINT('',(26.3,248.1,26.0213203435596)) ;
#88149=CARTESIAN_POINT('',(26.3,248.2,26.1213203435596)) ;
#88150=CARTESIAN_POINT('Origin',(28.,246.5,26.1213203435596)) ;
#88151=CARTESIAN_POINT('',(28.,246.4,26.1213203435596)) ;
#88152=CARTESIAN_POINT('',(28.1,246.5,26.1213203435596)) ;
#88153=CARTESIAN_POINT('Origin',(28.,246.5,26.1213203435596)) ;
#88154=CARTESIAN_POINT('',(28.,246.5,26.0213203435596)) ;
#88155=CARTESIAN_POINT('Origin',(28.,246.5,26.1213203435596)) ;
#88156=CARTESIAN_POINT('Origin',(28.,246.5,26.1213203435596)) ;
#88157=CARTESIAN_POINT('Origin',(26.4,246.5,26.1213203435596)) ;
#88158=CARTESIAN_POINT('',(26.3,246.5,26.1213203435596)) ;
#88159=CARTESIAN_POINT('',(26.4,246.4,26.1213203435596)) ;
#88160=CARTESIAN_POINT('Origin',(26.4,246.5,26.1213203435596)) ;
#88161=CARTESIAN_POINT('',(26.4,246.5,26.0213203435596)) ;
#88162=CARTESIAN_POINT('Origin',(26.4,246.5,26.1213203435596)) ;
#88163=CARTESIAN_POINT('Origin',(26.4,246.5,26.1213203435596)) ;
#88164=CARTESIAN_POINT('Origin',(26.4,246.85,26.1213203435596)) ;
#88165=CARTESIAN_POINT('',(26.3,246.85,26.1213203435596)) ;
#88166=CARTESIAN_POINT('',(26.4,246.85,26.0213203435596)) ;
#88167=CARTESIAN_POINT('Origin',(26.3,246.5,26.1213203435596)) ;
#88168=CARTESIAN_POINT('',(26.3,246.4,26.1213203435596)) ;
#88169=CARTESIAN_POINT('',(26.3,246.5,26.0213203435596)) ;
#88170=CARTESIAN_POINT('Origin',(26.4,246.5,26.5463203435596)) ;
#88171=CARTESIAN_POINT('',(26.4,246.4,26.7213203435596)) ;
#88172=CARTESIAN_POINT('',(26.3,246.5,26.7213203435596)) ;
#88173=CARTESIAN_POINT('Origin',(26.4,246.5,26.7213203435596)) ;
#88174=CARTESIAN_POINT('',(26.3,246.5,26.5463203435596)) ;
#88175=CARTESIAN_POINT('',(26.4,246.4,26.5463203435596)) ;
#88176=CARTESIAN_POINT('Origin',(28.,246.85,26.1213203435596)) ;
#88177=CARTESIAN_POINT('',(28.1,246.85,26.1213203435596)) ;
#88178=CARTESIAN_POINT('',(28.,246.85,26.0213203435596)) ;
#88179=CARTESIAN_POINT('Origin',(28.,246.5,26.5463203435596)) ;
#88180=CARTESIAN_POINT('',(28.,246.4,26.7213203435596)) ;
#88181=CARTESIAN_POINT('',(28.,246.4,26.5463203435596)) ;
#88182=CARTESIAN_POINT('',(28.1,246.5,26.6213203435596)) ;
#88183=CARTESIAN_POINT('',(28.1,246.5,26.5463203435596)) ;
#88184=CARTESIAN_POINT('Origin',(28.,246.5,26.6213203435596)) ;
#88185=CARTESIAN_POINT('Origin',(28.,248.1,26.1963203435596)) ;
#88186=CARTESIAN_POINT('',(28.1,248.1,26.1963203435596)) ;
#88187=CARTESIAN_POINT('',(28.,248.2,26.1963203435596)) ;
#88188=CARTESIAN_POINT('Origin',(28.,247.75,26.6213203435596)) ;
#88189=CARTESIAN_POINT('',(28.1,247.75,26.6213203435596)) ;
#88190=CARTESIAN_POINT('',(28.,247.75,26.7213203435596)) ;
#88191=CARTESIAN_POINT('Origin',(26.3,248.1,26.6213203435596)) ;
#88192=CARTESIAN_POINT('',(26.3,248.1,26.7213203435596)) ;
#88193=CARTESIAN_POINT('',(26.3,248.2,26.6213203435596)) ;
#88194=CARTESIAN_POINT('Origin',(26.3,247.3,26.3713203435596)) ;
#88195=CARTESIAN_POINT('',(26.3,247.7,26.7213203435596)) ;
#88196=CARTESIAN_POINT('Origin',(26.3,246.4,26.7213203435596)) ;
#88197=CARTESIAN_POINT('',(26.3,246.4,26.7213203435596)) ;
#88198=CARTESIAN_POINT('Origin',(26.3,248.2,26.0213203435596)) ;
#88199=CARTESIAN_POINT('Origin',(26.3,246.4,26.0213203435596)) ;
#88200=CARTESIAN_POINT('Origin',(28.1,247.3,26.3713203435596)) ;
#88201=CARTESIAN_POINT('Origin',(26.3,248.2,26.7213203435596)) ;
#117136=UNCERTAINTY_MEASURE_WITH_UNIT(LENGTH_MEASURE(0.01),#117171,
'DISTANCE_ACCURACY_VALUE',
'Maximum model space distance between geometric entities at asserted c
onnectivities') ;
#117147=UNCERTAINTY_MEASURE_WITH_UNIT(LENGTH_MEASURE(0.01),#117171,
'DISTANCE_ACCURACY_VALUE',
'Maximum model space distance between geometric entities at asserted c
onnectivities') ;
#117159=(
GEOMETRIC_REPRESENTATION_CONTEXT(3)
GLOBAL_UNCERTAINTY_ASSIGNED_CONTEXT((#117136))
GLOBAL_UNIT_ASSIGNED_CONTEXT((#117171,#117173,#117174))
REPRESENTATION_CONTEXT('','3D')
) ;
#117170=(
GEOMETRIC_REPRESENTATION_CONTEXT(3)
GLOBAL_UNCERTAINTY_ASSIGNED_CONTEXT((#117147))
GLOBAL_UNIT_ASSIGNED_CONTEXT((#117171,#117173,#117174))
REPRESENTATION_CONTEXT('','3D')
) ;
#117171=(
LENGTH_UNIT()
NAMED_UNIT(*)
SI_UNIT(.MILLI.,.METRE.)
) ;
#117173=(
NAMED_UNIT(*)
PLANE_ANGLE_UNIT()
SI_UNIT($,.RADIAN.)
) ;
#117174=(
NAMED_UNIT(*)
SI_UNIT($,.STERADIAN.)
SOLID_ANGLE_UNIT()
) ;
#117186=SHAPE_DEFINITION_REPRESENTATION(#117208,#117251) ;
#117208=PRODUCT_DEFINITION_SHAPE('',$,#117274) ;
#117251=SHAPE_REPRESENTATION('',(#52179),#117159) ;
#117262=PRODUCT_DEFINITION_CONTEXT('part definition',#117330,'design') ;
#117274=PRODUCT_DEFINITION('Washer_2','Washer_2',#117296,#117262) ;
#117296=PRODUCT_DEFINITION_FORMATION('',$,#117343) ;
#117330=APPLICATION_CONTEXT(
'Core Data for Automotive Mechanical Design Process') ;
#117331=PRODUCT_CONTEXT('part definition',#117330,'mechanical') ;
#117343=PRODUCT('Washer_2','Washer_2',$,(#117331)) ;
#117355=PRESENTATION_STYLE_ASSIGNMENT((#117357)) ;
#117357=SURFACE_STYLE_USAGE(.BOTH.,#117359) ;
#117359=SURFACE_SIDE_STYLE('',(#117361)) ;
#117361=SURFACE_STYLE_FILL_AREA(#117363) ;
#117363=FILL_AREA_STYLE('Opaque(160,160,160)',(#117365)) ;
#117365=FILL_AREA_STYLE_COLOUR('Opaque(160,160,160)',#117367) ;
#117367=COLOUR_RGB('Opaque(160,160,160)', 0.09019608, 0.27058824, 0.51372549) ;
ENDSEC;
END-ISO-10303-21;
